ISO-10303-21;
HEADER;
/* Generated by software containing ST-Developer
 * from STEP Tools, Inc. (www.steptools.com) 
 */

FILE_DESCRIPTION(
/* description */ ('Bin tilter linkage'),
/* implementation_level */ '2;1');

FILE_NAME(
/* name */ 'Cap Screw - M5x20.step',
/* time_stamp */ '2026-10-28T03:26:24-07:00',
/* author */ (''),
/* organization */ (''),
/* preprocessor_version */ 'ST-DEVELOPER v20.2',
/* originating_system */ 'Autodesk Translation Framework v15.17.0.0',
/* authorisation */ '');

FILE_SCHEMA (('AUTOMOTIVE_DESIGN { 1 0 10303 214 3 1 1 }'));
ENDSEC;

DATA;
#10=MECHANICAL_DESIGN_GEOMETRIC_PRESENTATION_REPRESENTATION('',(#891),#23728);
#629=ORIENTED_CLOSED_SHELL('',*,#12422,.F.);
#632=CONICAL_SURFACE('',#14178,0.4,0.785398163397448);
#633=CONICAL_SURFACE('',#14182,0.41,0.785398163397448);
#634=CONICAL_SURFACE('',#14186,0.26,0.463647609000806);
#635=CONICAL_SURFACE('',#14190,0.225,0.785398163397448);
#647=BREP_WITH_VOIDS('Body1',#12421,(#629));
#679=SHAPE_REPRESENTATION_RELATIONSHIP('SRR','None',#24143,#785);
#785=ADVANCED_BREP_SHAPE_REPRESENTATION('',(#647),#23643);
#891=STYLED_ITEM('',(#24772),#647);
#1233=FACE_BOUND('',#3050,.T.);
#1606=PLANE('',#14176);
#1607=PLANE('',#14184);
#1608=PLANE('',#14192);
#1609=PLANE('',#14193);
#1610=PLANE('',#14194);
#1611=PLANE('',#14195);
#1612=PLANE('',#14196);
#1613=PLANE('',#14197);
#1614=PLANE('',#14198);
#1615=PLANE('',#14199);
#1616=PLANE('',#14200);
#2122=FACE_OUTER_BOUND('',#3045,.T.);
#2123=FACE_OUTER_BOUND('',#3046,.T.);
#2124=FACE_OUTER_BOUND('',#3047,.T.);
#2125=FACE_OUTER_BOUND('',#3048,.T.);
#2126=FACE_OUTER_BOUND('',#3049,.T.);
#2127=FACE_OUTER_BOUND('',#3051,.T.);
#2128=FACE_OUTER_BOUND('',#3052,.T.);
#2129=FACE_OUTER_BOUND('',#3053,.T.);
#2130=FACE_OUTER_BOUND('',#3054,.T.);
#2131=FACE_OUTER_BOUND('',#3055,.T.);
#2132=FACE_OUTER_BOUND('',#3056,.T.);
#2133=FACE_OUTER_BOUND('',#3057,.T.);
#2134=FACE_OUTER_BOUND('',#3058,.T.);
#2135=FACE_OUTER_BOUND('',#3059,.T.);
#2136=FACE_OUTER_BOUND('',#3060,.T.);
#2137=FACE_OUTER_BOUND('',#3061,.T.);
#2138=FACE_OUTER_BOUND('',#3062,.T.);
#3045=EDGE_LOOP('',(#9309));
#3046=EDGE_LOOP('',(#9310,#9311,#9312,#9313));
#3047=EDGE_LOOP('',(#9314,#9315,#9316,#9317));
#3048=EDGE_LOOP('',(#9318,#9319,#9320,#9321));
#3049=EDGE_LOOP('',(#9322));
#3050=EDGE_LOOP('',(#9323));
#3051=EDGE_LOOP('',(#9324,#9325,#9326,#9327));
#3052=EDGE_LOOP('',(#9328,#9329,#9330,#9331));
#3053=EDGE_LOOP('',(#9332,#9333,#9334,#9335));
#3054=EDGE_LOOP('',(#9336));
#3055=EDGE_LOOP('',(#9337,#9338,#9339,#9340));
#3056=EDGE_LOOP('',(#9341,#9342,#9343,#9344));
#3057=EDGE_LOOP('',(#9345,#9346,#9347,#9348));
#3058=EDGE_LOOP('',(#9349,#9350,#9351,#9352));
#3059=EDGE_LOOP('',(#9353,#9354,#9355,#9356));
#3060=EDGE_LOOP('',(#9357,#9358,#9359,#9360));
#3061=EDGE_LOOP('',(#9361,#9362,#9363,#9364,#9365,#9366));
#3062=EDGE_LOOP('',(#9367,#9368,#9369,#9370,#9371,#9372));
#4081=LINE('',#20795,#4756);
#4082=LINE('',#20799,#4757);
#4083=LINE('',#20803,#4758);
#4084=LINE('',#20810,#4759);
#4085=LINE('',#20814,#4760);
#4086=LINE('',#20818,#4761);
#4087=LINE('',#20823,#4762);
#4088=LINE('',#20825,#4763);
#4089=LINE('',#20827,#4764);
#4090=LINE('',#20828,#4765);
#4091=LINE('',#20831,#4766);
#4092=LINE('',#20833,#4767);
#4093=LINE('',#20834,#4768);
#4094=LINE('',#20837,#4769);
#4095=LINE('',#20839,#4770);
#4096=LINE('',#20840,#4771);
#4097=LINE('',#20843,#4772);
#4098=LINE('',#20845,#4773);
#4099=LINE('',#20846,#4774);
#4100=LINE('',#20849,#4775);
#4101=LINE('',#20851,#4776);
#4102=LINE('',#20852,#4777);
#4103=LINE('',#20854,#4778);
#4104=LINE('',#20855,#4779);
#4756=VECTOR('',#16714,0.4);
#4757=VECTOR('',#16719,0.425);
#4758=VECTOR('',#16724,0.41);
#4759=VECTOR('',#16733,0.26);
#4760=VECTOR('',#16738,0.25);
#4761=VECTOR('',#16743,0.225);
#4762=VECTOR('',#16748,1.);
#4763=VECTOR('',#16749,1.);
#4764=VECTOR('',#16750,1.);
#4765=VECTOR('',#16751,1.);
#4766=VECTOR('',#16754,1.);
#4767=VECTOR('',#16755,1.);
#4768=VECTOR('',#16756,1.);
#4769=VECTOR('',#16759,1.);
#4770=VECTOR('',#16760,1.);
#4771=VECTOR('',#16761,1.);
#4772=VECTOR('',#16764,1.);
#4773=VECTOR('',#16765,1.);
#4774=VECTOR('',#16766,1.);
#4775=VECTOR('',#16769,1.);
#4776=VECTOR('',#16770,1.);
#4777=VECTOR('',#16771,1.);
#4778=VECTOR('',#16774,1.);
#4779=VECTOR('',#16775,1.);
#5435=CIRCLE('',#14177,0.375);
#5436=CIRCLE('',#14179,0.425);
#5437=CIRCLE('',#14181,0.425);
#5438=CIRCLE('',#14183,0.395);
#5439=CIRCLE('',#14185,0.27);
#5440=CIRCLE('',#14187,0.24505);
#5441=CIRCLE('',#14189,0.24505);
#5442=CIRCLE('',#14191,0.2);
#6269=VERTEX_POINT('',#20790);
#6270=VERTEX_POINT('',#20793);
#6271=VERTEX_POINT('',#20797);
#6272=VERTEX_POINT('',#20801);
#6273=VERTEX_POINT('',#20805);
#6274=VERTEX_POINT('',#20808);
#6275=VERTEX_POINT('',#20812);
#6276=VERTEX_POINT('',#20816);
#6277=VERTEX_POINT('',#20821);
#6278=VERTEX_POINT('',#20822);
#6279=VERTEX_POINT('',#20824);
#6280=VERTEX_POINT('',#20826);
#6281=VERTEX_POINT('',#20830);
#6282=VERTEX_POINT('',#20832);
#6283=VERTEX_POINT('',#20836);
#6284=VERTEX_POINT('',#20838);
#6285=VERTEX_POINT('',#20842);
#6286=VERTEX_POINT('',#20844);
#6287=VERTEX_POINT('',#20848);
#6288=VERTEX_POINT('',#20850);
#7394=EDGE_CURVE('',#6269,#6269,#5435,.T.);
#7395=EDGE_CURVE('',#6270,#6270,#5436,.T.);
#7396=EDGE_CURVE('',#6270,#6269,#4081,.T.);
#7397=EDGE_CURVE('',#6271,#6271,#5437,.T.);
#7398=EDGE_CURVE('',#6271,#6270,#4082,.T.);
#7399=EDGE_CURVE('',#6272,#6272,#5438,.T.);
#7400=EDGE_CURVE('',#6272,#6271,#4083,.T.);
#7401=EDGE_CURVE('',#6273,#6273,#5439,.T.);
#7402=EDGE_CURVE('',#6274,#6274,#5440,.F.);
#7403=EDGE_CURVE('',#6274,#6273,#4084,.T.);
#7404=EDGE_CURVE('',#6275,#6275,#5441,.F.);
#7405=EDGE_CURVE('',#6275,#6274,#4085,.T.);
#7406=EDGE_CURVE('',#6276,#6276,#5442,.T.);
#7407=EDGE_CURVE('',#6276,#6275,#4086,.T.);
#7408=EDGE_CURVE('',#6277,#6278,#4087,.T.);
#7409=EDGE_CURVE('',#6278,#6279,#4088,.T.);
#7410=EDGE_CURVE('',#6279,#6280,#4089,.T.);
#7411=EDGE_CURVE('',#6277,#6280,#4090,.T.);
#7412=EDGE_CURVE('',#6278,#6281,#4091,.T.);
#7413=EDGE_CURVE('',#6281,#6282,#4092,.T.);
#7414=EDGE_CURVE('',#6282,#6279,#4093,.T.);
#7415=EDGE_CURVE('',#6281,#6283,#4094,.T.);
#7416=EDGE_CURVE('',#6283,#6284,#4095,.T.);
#7417=EDGE_CURVE('',#6284,#6282,#4096,.T.);
#7418=EDGE_CURVE('',#6283,#6285,#4097,.T.);
#7419=EDGE_CURVE('',#6285,#6286,#4098,.T.);
#7420=EDGE_CURVE('',#6286,#6284,#4099,.T.);
#7421=EDGE_CURVE('',#6285,#6287,#4100,.T.);
#7422=EDGE_CURVE('',#6287,#6288,#4101,.T.);
#7423=EDGE_CURVE('',#6288,#6286,#4102,.T.);
#7424=EDGE_CURVE('',#6287,#6277,#4103,.T.);
#7425=EDGE_CURVE('',#6280,#6288,#4104,.T.);
#9309=ORIENTED_EDGE('',*,*,#7394,.F.);
#9310=ORIENTED_EDGE('',*,*,#7395,.F.);
#9311=ORIENTED_EDGE('',*,*,#7396,.T.);
#9312=ORIENTED_EDGE('',*,*,#7394,.T.);
#9313=ORIENTED_EDGE('',*,*,#7396,.F.);
#9314=ORIENTED_EDGE('',*,*,#7397,.F.);
#9315=ORIENTED_EDGE('',*,*,#7398,.T.);
#9316=ORIENTED_EDGE('',*,*,#7395,.T.);
#9317=ORIENTED_EDGE('',*,*,#7398,.F.);
#9318=ORIENTED_EDGE('',*,*,#7399,.F.);
#9319=ORIENTED_EDGE('',*,*,#7400,.T.);
#9320=ORIENTED_EDGE('',*,*,#7397,.T.);
#9321=ORIENTED_EDGE('',*,*,#7400,.F.);
#9322=ORIENTED_EDGE('',*,*,#7399,.T.);
#9323=ORIENTED_EDGE('',*,*,#7401,.F.);
#9324=ORIENTED_EDGE('',*,*,#7402,.F.);
#9325=ORIENTED_EDGE('',*,*,#7403,.T.);
#9326=ORIENTED_EDGE('',*,*,#7401,.T.);
#9327=ORIENTED_EDGE('',*,*,#7403,.F.);
#9328=ORIENTED_EDGE('',*,*,#7404,.F.);
#9329=ORIENTED_EDGE('',*,*,#7405,.T.);
#9330=ORIENTED_EDGE('',*,*,#7402,.T.);
#9331=ORIENTED_EDGE('',*,*,#7405,.F.);
#9332=ORIENTED_EDGE('',*,*,#7406,.F.);
#9333=ORIENTED_EDGE('',*,*,#7407,.T.);
#9334=ORIENTED_EDGE('',*,*,#7404,.T.);
#9335=ORIENTED_EDGE('',*,*,#7407,.F.);
#9336=ORIENTED_EDGE('',*,*,#7406,.T.);
#9337=ORIENTED_EDGE('',*,*,#7408,.T.);
#9338=ORIENTED_EDGE('',*,*,#7409,.T.);
#9339=ORIENTED_EDGE('',*,*,#7410,.T.);
#9340=ORIENTED_EDGE('',*,*,#7411,.F.);
#9341=ORIENTED_EDGE('',*,*,#7412,.T.);
#9342=ORIENTED_EDGE('',*,*,#7413,.T.);
#9343=ORIENTED_EDGE('',*,*,#7414,.T.);
#9344=ORIENTED_EDGE('',*,*,#7409,.F.);
#9345=ORIENTED_EDGE('',*,*,#7415,.T.);
#9346=ORIENTED_EDGE('',*,*,#7416,.T.);
#9347=ORIENTED_EDGE('',*,*,#7417,.T.);
#9348=ORIENTED_EDGE('',*,*,#7413,.F.);
#9349=ORIENTED_EDGE('',*,*,#7418,.T.);
#9350=ORIENTED_EDGE('',*,*,#7419,.T.);
#9351=ORIENTED_EDGE('',*,*,#7420,.T.);
#9352=ORIENTED_EDGE('',*,*,#7416,.F.);
#9353=ORIENTED_EDGE('',*,*,#7421,.T.);
#9354=ORIENTED_EDGE('',*,*,#7422,.T.);
#9355=ORIENTED_EDGE('',*,*,#7423,.T.);
#9356=ORIENTED_EDGE('',*,*,#7419,.F.);
#9357=ORIENTED_EDGE('',*,*,#7424,.T.);
#9358=ORIENTED_EDGE('',*,*,#7411,.T.);
#9359=ORIENTED_EDGE('',*,*,#7425,.T.);
#9360=ORIENTED_EDGE('',*,*,#7422,.F.);
#9361=ORIENTED_EDGE('',*,*,#7424,.F.);
#9362=ORIENTED_EDGE('',*,*,#7421,.F.);
#9363=ORIENTED_EDGE('',*,*,#7418,.F.);
#9364=ORIENTED_EDGE('',*,*,#7415,.F.);
#9365=ORIENTED_EDGE('',*,*,#7412,.F.);
#9366=ORIENTED_EDGE('',*,*,#7408,.F.);
#9367=ORIENTED_EDGE('',*,*,#7425,.F.);
#9368=ORIENTED_EDGE('',*,*,#7410,.F.);
#9369=ORIENTED_EDGE('',*,*,#7414,.F.);
#9370=ORIENTED_EDGE('',*,*,#7417,.F.);
#9371=ORIENTED_EDGE('',*,*,#7420,.F.);
#9372=ORIENTED_EDGE('',*,*,#7423,.F.);
#11385=CYLINDRICAL_SURFACE('',#14180,0.425);
#11386=CYLINDRICAL_SURFACE('',#14188,0.24505);
#11847=ADVANCED_FACE('',(#2122),#1606,.T.);
#11848=ADVANCED_FACE('',(#2123),#632,.T.);
#11849=ADVANCED_FACE('',(#2124),#11385,.T.);
#11850=ADVANCED_FACE('',(#2125),#633,.T.);
#11851=ADVANCED_FACE('',(#2126,#1233),#1607,.T.);
#11852=ADVANCED_FACE('',(#2127),#634,.T.);
#11853=ADVANCED_FACE('',(#2128),#11386,.T.);
#11854=ADVANCED_FACE('',(#2129),#635,.T.);
#11855=ADVANCED_FACE('',(#2130),#1608,.T.);
#11856=ADVANCED_FACE('',(#2131),#1609,.F.);
#11857=ADVANCED_FACE('',(#2132),#1610,.F.);
#11858=ADVANCED_FACE('',(#2133),#1611,.F.);
#11859=ADVANCED_FACE('',(#2134),#1612,.F.);
#11860=ADVANCED_FACE('',(#2135),#1613,.F.);
#11861=ADVANCED_FACE('',(#2136),#1614,.F.);
#11862=ADVANCED_FACE('',(#2137),#1615,.F.);
#11863=ADVANCED_FACE('',(#2138),#1616,.F.);
#12421=CLOSED_SHELL('',(#11847,#11848,#11849,#11850,#11851,#11852,#11853,
#11854,#11855));
#12422=CLOSED_SHELL('',(#11856,#11857,#11858,#11859,#11860,#11861,#11862,
#11863));
#14175=AXIS2_PLACEMENT_3D('',#20788,#16704,#16705);
#14176=AXIS2_PLACEMENT_3D('',#20789,#16706,#16707);
#14177=AXIS2_PLACEMENT_3D('',#20791,#16708,#16709);
#14178=AXIS2_PLACEMENT_3D('',#20792,#16710,#16711);
#14179=AXIS2_PLACEMENT_3D('',#20794,#16712,#16713);
#14180=AXIS2_PLACEMENT_3D('',#20796,#16715,#16716);
#14181=AXIS2_PLACEMENT_3D('',#20798,#16717,#16718);
#14182=AXIS2_PLACEMENT_3D('',#20800,#16720,#16721);
#14183=AXIS2_PLACEMENT_3D('',#20802,#16722,#16723);
#14184=AXIS2_PLACEMENT_3D('',#20804,#16725,#16726);
#14185=AXIS2_PLACEMENT_3D('',#20806,#16727,#16728);
#14186=AXIS2_PLACEMENT_3D('',#20807,#16729,#16730);
#14187=AXIS2_PLACEMENT_3D('',#20809,#16731,#16732);
#14188=AXIS2_PLACEMENT_3D('',#20811,#16734,#16735);
#14189=AXIS2_PLACEMENT_3D('',#20813,#16736,#16737);
#14190=AXIS2_PLACEMENT_3D('',#20815,#16739,#16740);
#14191=AXIS2_PLACEMENT_3D('',#20817,#16741,#16742);
#14192=AXIS2_PLACEMENT_3D('',#20819,#16744,#16745);
#14193=AXIS2_PLACEMENT_3D('',#20820,#16746,#16747);
#14194=AXIS2_PLACEMENT_3D('',#20829,#16752,#16753);
#14195=AXIS2_PLACEMENT_3D('',#20835,#16757,#16758);
#14196=AXIS2_PLACEMENT_3D('',#20841,#16762,#16763);
#14197=AXIS2_PLACEMENT_3D('',#20847,#16767,#16768);
#14198=AXIS2_PLACEMENT_3D('',#20853,#16772,#16773);
#14199=AXIS2_PLACEMENT_3D('',#20856,#16776,#16777);
#14200=AXIS2_PLACEMENT_3D('',#20857,#16778,#16779);
#16704=DIRECTION('axis',(0.,0.,1.));
#16705=DIRECTION('refdir',(1.,0.,0.));
#16706=DIRECTION('center_axis',(0.,1.,0.));
#16707=DIRECTION('ref_axis',(0.,0.,1.));
#16708=DIRECTION('center_axis',(0.,-1.,0.));
#16709=DIRECTION('ref_axis',(1.,0.,0.));
#16710=DIRECTION('center_axis',(0.,-1.,0.));
#16711=DIRECTION('ref_axis',(1.,0.,0.));
#16712=DIRECTION('center_axis',(0.,-1.,0.));
#16713=DIRECTION('ref_axis',(1.,0.,0.));
#16714=DIRECTION('',(0.707106781186548,0.707106781186547,8.65956056235493E-17));
#16715=DIRECTION('center_axis',(0.,-1.,0.));
#16716=DIRECTION('ref_axis',(1.,0.,0.));
#16717=DIRECTION('center_axis',(0.,-1.,0.));
#16718=DIRECTION('ref_axis',(1.,0.,0.));
#16719=DIRECTION('',(0.,1.,0.));
#16720=DIRECTION('center_axis',(0.,1.,0.));
#16721=DIRECTION('ref_axis',(1.,0.,0.));
#16722=DIRECTION('center_axis',(0.,-1.,0.));
#16723=DIRECTION('ref_axis',(1.,0.,0.));
#16724=DIRECTION('',(-0.707106781186547,0.707106781186548,-8.65956056235493E-17));
#16725=DIRECTION('center_axis',(0.,-1.,0.));
#16726=DIRECTION('ref_axis',(0.,0.,-1.));
#16727=DIRECTION('center_axis',(0.,-1.,0.));
#16728=DIRECTION('ref_axis',(1.,0.,0.));
#16729=DIRECTION('center_axis',(0.,1.,0.));
#16730=DIRECTION('ref_axis',(1.,0.,0.));
#16731=DIRECTION('center_axis',(0.,1.,0.));
#16732=DIRECTION('ref_axis',(1.,0.,0.));
#16733=DIRECTION('',(-0.447213595499958,0.894427190999916,-5.47678698264203E-17));
#16734=DIRECTION('center_axis',(0.,-1.,0.));
#16735=DIRECTION('ref_axis',(1.,0.,0.));
#16736=DIRECTION('center_axis',(0.,1.,0.));
#16737=DIRECTION('ref_axis',(1.,0.,0.));
#16738=DIRECTION('',(0.,1.,0.));
#16739=DIRECTION('center_axis',(0.,1.,0.));
#16740=DIRECTION('ref_axis',(1.,0.,0.));
#16741=DIRECTION('center_axis',(0.,-1.,0.));
#16742=DIRECTION('ref_axis',(1.,0.,0.));
#16743=DIRECTION('',(-0.707106781186547,0.707106781186548,-8.65956056235493E-17));
#16744=DIRECTION('center_axis',(0.,-1.,0.));
#16745=DIRECTION('ref_axis',(0.,0.,-1.));
#16746=DIRECTION('center_axis',(0.866025403784439,0.,-0.5));
#16747=DIRECTION('ref_axis',(0.5,0.,0.866025403784439));
#16748=DIRECTION('',(-0.5,0.,-0.866025403784439));
#16749=DIRECTION('',(0.,-1.,0.));
#16750=DIRECTION('',(0.5,0.,0.866025403784439));
#16751=DIRECTION('',(0.,-1.,0.));
#16752=DIRECTION('center_axis',(1.20185167898973E-16,0.,-1.));
#16753=DIRECTION('ref_axis',(1.,0.,1.20185167898973E-16));
#16754=DIRECTION('',(-1.,0.,-1.20185167898973E-16));
#16755=DIRECTION('',(0.,-1.,0.));
#16756=DIRECTION('',(1.,0.,1.20185167898973E-16));
#16757=DIRECTION('center_axis',(-0.866025403784439,0.,-0.5));
#16758=DIRECTION('ref_axis',(0.5,0.,-0.866025403784439));
#16759=DIRECTION('',(-0.5,0.,0.866025403784439));
#16760=DIRECTION('',(0.,-1.,0.));
#16761=DIRECTION('',(0.5,0.,-0.866025403784439));
#16762=DIRECTION('center_axis',(-0.866025403784439,0.,0.5));
#16763=DIRECTION('ref_axis',(-0.5,0.,-0.866025403784439));
#16764=DIRECTION('',(0.5,0.,0.866025403784439));
#16765=DIRECTION('',(0.,-1.,0.));
#16766=DIRECTION('',(-0.5,0.,-0.866025403784439));
#16767=DIRECTION('center_axis',(-2.40370335797945E-16,0.,1.));
#16768=DIRECTION('ref_axis',(-1.,0.,-2.40370335797945E-16));
#16769=DIRECTION('',(1.,0.,2.40370335797945E-16));
#16770=DIRECTION('',(0.,-1.,0.));
#16771=DIRECTION('',(-1.,0.,-2.40370335797945E-16));
#16772=DIRECTION('center_axis',(0.866025403784439,0.,0.5));
#16773=DIRECTION('ref_axis',(-0.5,0.,0.866025403784439));
#16774=DIRECTION('',(0.5,0.,-0.866025403784439));
#16775=DIRECTION('',(-0.5,0.,0.866025403784439));
#16776=DIRECTION('center_axis',(0.,1.,0.));
#16777=DIRECTION('ref_axis',(1.,0.,0.));
#16778=DIRECTION('center_axis',(0.,-1.,0.));
#16779=DIRECTION('ref_axis',(0.,0.,-1.));
#20788=CARTESIAN_POINT('',(0.,0.,0.));
#20789=CARTESIAN_POINT('Origin',(0.375,0.5,0.));
#20790=CARTESIAN_POINT('',(-0.375,0.5,-4.59242549680257E-17));
#20791=CARTESIAN_POINT('Origin',(0.,0.5,0.));
#20792=CARTESIAN_POINT('Origin',(0.,0.475,0.));
#20793=CARTESIAN_POINT('',(-0.425,0.45,-5.20474889637625E-17));
#20794=CARTESIAN_POINT('Origin',(0.,0.45,0.));
#20795=CARTESIAN_POINT('',(-0.4,0.475,-4.89858719658941E-17));
#20796=CARTESIAN_POINT('Origin',(0.,0.24,0.));
#20797=CARTESIAN_POINT('',(-0.425,0.0299999999999998,-5.20474889637625E-17));
#20798=CARTESIAN_POINT('Origin',(0.,0.0299999999999998,0.));
#20799=CARTESIAN_POINT('',(-0.425,0.24,-5.20474889637625E-17));
#20800=CARTESIAN_POINT('Origin',(0.,0.0150000000000001,0.));
#20801=CARTESIAN_POINT('',(-0.395,4.85722573273506E-17,-4.83735485663204E-17));
#20802=CARTESIAN_POINT('Origin',(0.,0.,0.));
#20803=CARTESIAN_POINT('',(-0.41,0.0150000000000001,-5.02105187650415E-17));
#20804=CARTESIAN_POINT('Origin',(0.27,0.,0.));
#20805=CARTESIAN_POINT('',(-0.27,0.,-3.30654635769785E-17));
#20806=CARTESIAN_POINT('Origin',(0.,0.,0.));
#20807=CARTESIAN_POINT('Origin',(0.,-0.02,0.));
#20808=CARTESIAN_POINT('',(-0.24505,-0.0498999999999999,3.00099698131059E-17));
#20809=CARTESIAN_POINT('Origin',(0.,-0.0498999999999999,0.));
#20810=CARTESIAN_POINT('',(-0.26,-0.02,-3.18408167778312E-17));
#20811=CARTESIAN_POINT('Origin',(0.,-0.995,0.));
#20812=CARTESIAN_POINT('',(-0.24505,-1.95495,3.00099698131059E-17));
#20813=CARTESIAN_POINT('Origin',(0.,-1.95495,0.));
#20814=CARTESIAN_POINT('',(-0.24505,-0.995,-3.00099698131059E-17));
#20815=CARTESIAN_POINT('Origin',(0.,-1.975,0.));
#20816=CARTESIAN_POINT('',(-0.2,-2.,-2.44929359829471E-17));
#20817=CARTESIAN_POINT('Origin',(0.,-2.,0.));
#20818=CARTESIAN_POINT('',(-0.225,-1.975,-2.75545529808154E-17));
#20819=CARTESIAN_POINT('Origin',(0.,-2.,0.));
#20820=CARTESIAN_POINT('Origin',(0.115470053837925,-0.5,-0.2));
#20821=CARTESIAN_POINT('',(0.23094010767585,-0.5,0.));
#20822=CARTESIAN_POINT('',(0.115470053837925,-0.5,-0.2));
#20823=CARTESIAN_POINT('',(0.23094010767585,-0.5,0.));
#20824=CARTESIAN_POINT('',(0.115470053837925,-0.8,-0.2));
#20825=CARTESIAN_POINT('',(0.115470053837925,-0.5,-0.2));
#20826=CARTESIAN_POINT('',(0.23094010767585,-0.8,0.));
#20827=CARTESIAN_POINT('',(0.23094010767585,-0.8,0.));
#20828=CARTESIAN_POINT('',(0.23094010767585,-0.5,0.));
#20829=CARTESIAN_POINT('Origin',(-0.115470053837925,-0.5,-0.2));
#20830=CARTESIAN_POINT('',(-0.115470053837925,-0.5,-0.2));
#20831=CARTESIAN_POINT('',(0.115470053837925,-0.5,-0.2));
#20832=CARTESIAN_POINT('',(-0.115470053837925,-0.8,-0.2));
#20833=CARTESIAN_POINT('',(-0.115470053837925,-0.5,-0.2));
#20834=CARTESIAN_POINT('',(0.115470053837925,-0.8,-0.2));
#20835=CARTESIAN_POINT('Origin',(-0.23094010767585,-0.5,-2.77555756156289E-17));
#20836=CARTESIAN_POINT('',(-0.23094010767585,-0.5,-2.82820063659975E-17));
#20837=CARTESIAN_POINT('',(-0.115470053837925,-0.5,-0.2));
#20838=CARTESIAN_POINT('',(-0.23094010767585,-0.8,-2.77555756156289E-17));
#20839=CARTESIAN_POINT('',(-0.23094010767585,-0.5,-2.82820063659975E-17));
#20840=CARTESIAN_POINT('',(-0.115470053837925,-0.8,-0.2));
#20841=CARTESIAN_POINT('Origin',(-0.115470053837925,-0.5,0.2));
#20842=CARTESIAN_POINT('',(-0.115470053837925,-0.5,0.2));
#20843=CARTESIAN_POINT('',(-0.23094010767585,-0.5,-2.82820063659975E-17));
#20844=CARTESIAN_POINT('',(-0.115470053837925,-0.8,0.2));
#20845=CARTESIAN_POINT('',(-0.115470053837925,-0.5,0.2));
#20846=CARTESIAN_POINT('',(-0.23094010767585,-0.8,-2.82820063659975E-17));
#20847=CARTESIAN_POINT('Origin',(0.115470053837925,-0.5,0.2));
#20848=CARTESIAN_POINT('',(0.115470053837925,-0.5,0.2));
#20849=CARTESIAN_POINT('',(-0.115470053837925,-0.5,0.2));
#20850=CARTESIAN_POINT('',(0.115470053837925,-0.8,0.2));
#20851=CARTESIAN_POINT('',(0.115470053837925,-0.5,0.2));
#20852=CARTESIAN_POINT('',(-0.115470053837925,-0.8,0.2));
#20853=CARTESIAN_POINT('Origin',(0.23094010767585,-0.5,0.));
#20854=CARTESIAN_POINT('',(0.115470053837925,-0.5,0.2));
#20855=CARTESIAN_POINT('',(0.115470053837925,-0.8,0.2));
#20856=CARTESIAN_POINT('Origin',(0.,-0.5,0.));
#20857=CARTESIAN_POINT('Origin',(0.,-0.8,0.));
#23526=UNCERTAINTY_MEASURE_WITH_UNIT(LENGTH_MEASURE(0.001),#23729,
'DISTANCE_ACCURACY_VALUE',
'Maximum model space distance between geometric entities at asserted c
onnectivities');
#23611=UNCERTAINTY_MEASURE_WITH_UNIT(LENGTH_MEASURE(0.001),#23729,
'DISTANCE_ACCURACY_VALUE',
'Maximum model space distance between geometric entities at asserted c
onnectivities');
#23643=(
GEOMETRIC_REPRESENTATION_CONTEXT(3)
GLOBAL_UNCERTAINTY_ASSIGNED_CONTEXT((#23526))
GLOBAL_UNIT_ASSIGNED_CONTEXT((#23729,#23731,#23732))
REPRESENTATION_CONTEXT('','3D')
);
#23728=(
GEOMETRIC_REPRESENTATION_CONTEXT(3)
GLOBAL_UNCERTAINTY_ASSIGNED_CONTEXT((#23611))
GLOBAL_UNIT_ASSIGNED_CONTEXT((#23729,#23731,#23732))
REPRESENTATION_CONTEXT('','3D')
);
#23729=(
LENGTH_UNIT()
NAMED_UNIT(*)
SI_UNIT(.CENTI.,.METRE.)
);
#23731=(
NAMED_UNIT(*)
PLANE_ANGLE_UNIT()
SI_UNIT($,.RADIAN.)
);
#23732=(
NAMED_UNIT(*)
SI_UNIT($,.STERADIAN.)
SOLID_ANGLE_UNIT()
);
#23764=SHAPE_DEFINITION_REPRESENTATION(#23880,#24143);
#23880=PRODUCT_DEFINITION_SHAPE('',$,#24260);
#24143=SHAPE_REPRESENTATION('',(#14175),#23643);
#24228=PRODUCT_DEFINITION_CONTEXT('part definition',#24578,'design');
#24260=PRODUCT_DEFINITION('Cap Screw - M5x20','Cap Screw - M5x20',#24376,
#24228);
#24376=PRODUCT_DEFINITION_FORMATION('',$,#24611);
#24578=APPLICATION_CONTEXT(
'Core Data for Automotive Mechanical Design Process');
#24579=PRODUCT_CONTEXT('part definition',#24578,'mechanical');
#24611=PRODUCT('Cap Screw - M5x20','Cap Screw - M5x20',
'Cap Screw - M5x20',(#24579));
#24766=COLOUR_RGB('Black',0.12,0.14,0.17);
#24767=FILL_AREA_STYLE_COLOUR('',#24766);
#24768=FILL_AREA_STYLE('',(#24767));
#24769=SURFACE_STYLE_FILL_AREA(#24768);
#24770=SURFACE_SIDE_STYLE('',(#24769));
#24771=SURFACE_STYLE_USAGE(.BOTH.,#24770);
#24772=PRESENTATION_STYLE_ASSIGNMENT((#24771));
ENDSEC;
END-ISO-10303-21;
